ISO-10303-21;
HEADER;
/* Generated by software containing ST-Developer
 * from STEP Tools, Inc. (www.steptools.com) 
 */

FILE_DESCRIPTION(
/* description */ ('Dual-rail gantry carriage'),
/* implementation_level */ '2;1');

FILE_NAME(
/* name */ 'M4x10 Cap Screw.step',
/* time_stamp */ '2026-10-27T10:49:15-07:00',
/* author */ (''),
/* organization */ (''),
/* preprocessor_version */ 'ST-DEVELOPER v20.2',
/* originating_system */ 'Autodesk Translation Framework v15.17.0.0',
/* authorisation */ '');

FILE_SCHEMA (('AUTOMOTIVE_DESIGN { 1 0 10303 214 3 1 1 }'));
ENDSEC;

DATA;
#10=MECHANICAL_DESIGN_GEOMETRIC_PRESENTATION_REPRESENTATION('',(#615),#12804);
#497=ORIENTED_CLOSED_SHELL('',*,#7397,.F.);
#515=CONICAL_SURFACE('',#8429,0.325,0.785398163397448);
#516=CONICAL_SURFACE('',#8433,0.335,0.785398163397448);
#517=CONICAL_SURFACE('',#8437,0.21,0.463647609000806);
#522=BREP_WITH_VOIDS('Body1',#7398,(#497));
#553=SHAPE_REPRESENTATION_RELATIONSHIP('SRR','None',#13033,#584);
#584=ADVANCED_BREP_SHAPE_REPRESENTATION('',(#522),#12803);
#615=STYLED_ITEM('',(#13254),#522);
#763=FACE_BOUND('',#1945,.T.);
#1037=PLANE('',#8417);
#1038=PLANE('',#8418);
#1039=PLANE('',#8419);
#1040=PLANE('',#8420);
#1041=PLANE('',#8421);
#1042=PLANE('',#8422);
#1043=PLANE('',#8423);
#1044=PLANE('',#8424);
#1045=PLANE('',#8425);
#1046=PLANE('',#8427);
#1047=PLANE('',#8435);
#1421=FACE_OUTER_BOUND('',#1931,.T.);
#1422=FACE_OUTER_BOUND('',#1932,.T.);
#1423=FACE_OUTER_BOUND('',#1933,.T.);
#1424=FACE_OUTER_BOUND('',#1934,.T.);
#1425=FACE_OUTER_BOUND('',#1935,.T.);
#1426=FACE_OUTER_BOUND('',#1936,.T.);
#1427=FACE_OUTER_BOUND('',#1937,.T.);
#1428=FACE_OUTER_BOUND('',#1938,.T.);
#1429=FACE_OUTER_BOUND('',#1939,.T.);
#1430=FACE_OUTER_BOUND('',#1940,.T.);
#1431=FACE_OUTER_BOUND('',#1941,.T.);
#1432=FACE_OUTER_BOUND('',#1942,.T.);
#1433=FACE_OUTER_BOUND('',#1943,.T.);
#1434=FACE_OUTER_BOUND('',#1944,.T.);
#1435=FACE_OUTER_BOUND('',#1946,.T.);
#1436=FACE_OUTER_BOUND('',#1947,.T.);
#1931=EDGE_LOOP('',(#6829,#6830,#6831,#6832));
#1932=EDGE_LOOP('',(#6833,#6834,#6835,#6836));
#1933=EDGE_LOOP('',(#6837,#6838,#6839,#6840));
#1934=EDGE_LOOP('',(#6841,#6842,#6843,#6844));
#1935=EDGE_LOOP('',(#6845,#6846,#6847,#6848));
#1936=EDGE_LOOP('',(#6849,#6850,#6851,#6852));
#1937=EDGE_LOOP('',(#6853,#6854,#6855,#6856,#6857,#6858));
#1938=EDGE_LOOP('',(#6859,#6860,#6861,#6862,#6863,#6864));
#1939=EDGE_LOOP('',(#6865));
#1940=EDGE_LOOP('',(#6866));
#1941=EDGE_LOOP('',(#6867,#6868,#6869,#6870));
#1942=EDGE_LOOP('',(#6871,#6872,#6873,#6874));
#1943=EDGE_LOOP('',(#6875,#6876,#6877,#6878));
#1944=EDGE_LOOP('',(#6879));
#1945=EDGE_LOOP('',(#6880));
#1946=EDGE_LOOP('',(#6881,#6882,#6883,#6884));
#1947=EDGE_LOOP('',(#6885,#6886,#6887,#6888));
#2634=LINE('',#12624,#3343);
#2635=LINE('',#12626,#3344);
#2636=LINE('',#12628,#3345);
#2637=LINE('',#12629,#3346);
#2638=LINE('',#12632,#3347);
#2639=LINE('',#12634,#3348);
#2640=LINE('',#12635,#3349);
#2641=LINE('',#12638,#3350);
#2642=LINE('',#12640,#3351);
#2643=LINE('',#12641,#3352);
#2644=LINE('',#12644,#3353);
#2645=LINE('',#12646,#3354);
#2646=LINE('',#12647,#3355);
#2647=LINE('',#12650,#3356);
#2648=LINE('',#12652,#3357);
#2649=LINE('',#12653,#3358);
#2650=LINE('',#12655,#3359);
#2651=LINE('',#12656,#3360);
#2652=LINE('',#12668,#3361);
#2653=LINE('',#12672,#3362);
#2654=LINE('',#12676,#3363);
#2655=LINE('',#12683,#3364);
#2656=LINE('',#12685,#3365);
#3343=VECTOR('',#10527,1.);
#3344=VECTOR('',#10528,1.);
#3345=VECTOR('',#10529,1.);
#3346=VECTOR('',#10530,1.);
#3347=VECTOR('',#10533,1.);
#3348=VECTOR('',#10534,1.);
#3349=VECTOR('',#10535,1.);
#3350=VECTOR('',#10538,1.);
#3351=VECTOR('',#10539,1.);
#3352=VECTOR('',#10540,1.);
#3353=VECTOR('',#10543,1.);
#3354=VECTOR('',#10544,1.);
#3355=VECTOR('',#10545,1.);
#3356=VECTOR('',#10548,1.);
#3357=VECTOR('',#10549,1.);
#3358=VECTOR('',#10550,1.);
#3359=VECTOR('',#10553,1.);
#3360=VECTOR('',#10554,1.);
#3361=VECTOR('',#10571,0.325);
#3362=VECTOR('',#10576,0.35);
#3363=VECTOR('',#10581,0.335);
#3364=VECTOR('',#10590,0.21);
#3365=VECTOR('',#10593,0.2);
#3559=CIRCLE('',#8426,0.1954);
#3560=CIRCLE('',#8428,0.3);
#3561=CIRCLE('',#8430,0.35);
#3562=CIRCLE('',#8432,0.35);
#3563=CIRCLE('',#8434,0.32);
#3564=CIRCLE('',#8436,0.22);
#3565=CIRCLE('',#8438,0.1954);
#4137=VERTEX_POINT('',#12622);
#4138=VERTEX_POINT('',#12623);
#4139=VERTEX_POINT('',#12625);
#4140=VERTEX_POINT('',#12627);
#4141=VERTEX_POINT('',#12631);
#4142=VERTEX_POINT('',#12633);
#4143=VERTEX_POINT('',#12637);
#4144=VERTEX_POINT('',#12639);
#4145=VERTEX_POINT('',#12643);
#4146=VERTEX_POINT('',#12645);
#4147=VERTEX_POINT('',#12649);
#4148=VERTEX_POINT('',#12651);
#4149=VERTEX_POINT('',#12660);
#4150=VERTEX_POINT('',#12663);
#4151=VERTEX_POINT('',#12666);
#4152=VERTEX_POINT('',#12670);
#4153=VERTEX_POINT('',#12674);
#4154=VERTEX_POINT('',#12678);
#4155=VERTEX_POINT('',#12681);
#5037=EDGE_CURVE('',#4137,#4138,#2634,.T.);
#5038=EDGE_CURVE('',#4138,#4139,#2635,.T.);
#5039=EDGE_CURVE('',#4139,#4140,#2636,.T.);
#5040=EDGE_CURVE('',#4137,#4140,#2637,.T.);
#5041=EDGE_CURVE('',#4138,#4141,#2638,.T.);
#5042=EDGE_CURVE('',#4141,#4142,#2639,.T.);
#5043=EDGE_CURVE('',#4142,#4139,#2640,.T.);
#5044=EDGE_CURVE('',#4141,#4143,#2641,.T.);
#5045=EDGE_CURVE('',#4143,#4144,#2642,.T.);
#5046=EDGE_CURVE('',#4144,#4142,#2643,.T.);
#5047=EDGE_CURVE('',#4143,#4145,#2644,.T.);
#5048=EDGE_CURVE('',#4145,#4146,#2645,.T.);
#5049=EDGE_CURVE('',#4146,#4144,#2646,.T.);
#5050=EDGE_CURVE('',#4145,#4147,#2647,.T.);
#5051=EDGE_CURVE('',#4147,#4148,#2648,.T.);
#5052=EDGE_CURVE('',#4148,#4146,#2649,.T.);
#5053=EDGE_CURVE('',#4147,#4137,#2650,.T.);
#5054=EDGE_CURVE('',#4140,#4148,#2651,.T.);
#5055=EDGE_CURVE('',#4149,#4149,#3559,.T.);
#5056=EDGE_CURVE('',#4150,#4150,#3560,.T.);
#5057=EDGE_CURVE('',#4151,#4151,#3561,.T.);
#5058=EDGE_CURVE('',#4151,#4150,#2652,.T.);
#5059=EDGE_CURVE('',#4152,#4152,#3562,.T.);
#5060=EDGE_CURVE('',#4152,#4151,#2653,.T.);
#5061=EDGE_CURVE('',#4153,#4153,#3563,.T.);
#5062=EDGE_CURVE('',#4153,#4152,#2654,.T.);
#5063=EDGE_CURVE('',#4154,#4154,#3564,.T.);
#5064=EDGE_CURVE('',#4155,#4155,#3565,.F.);
#5065=EDGE_CURVE('',#4155,#4154,#2655,.T.);
#5066=EDGE_CURVE('',#4149,#4155,#2656,.T.);
#6829=ORIENTED_EDGE('',*,*,#5037,.T.);
#6830=ORIENTED_EDGE('',*,*,#5038,.T.);
#6831=ORIENTED_EDGE('',*,*,#5039,.T.);
#6832=ORIENTED_EDGE('',*,*,#5040,.F.);
#6833=ORIENTED_EDGE('',*,*,#5041,.T.);
#6834=ORIENTED_EDGE('',*,*,#5042,.T.);
#6835=ORIENTED_EDGE('',*,*,#5043,.T.);
#6836=ORIENTED_EDGE('',*,*,#5038,.F.);
#6837=ORIENTED_EDGE('',*,*,#5044,.T.);
#6838=ORIENTED_EDGE('',*,*,#5045,.T.);
#6839=ORIENTED_EDGE('',*,*,#5046,.T.);
#6840=ORIENTED_EDGE('',*,*,#5042,.F.);
#6841=ORIENTED_EDGE('',*,*,#5047,.T.);
#6842=ORIENTED_EDGE('',*,*,#5048,.T.);
#6843=ORIENTED_EDGE('',*,*,#5049,.T.);
#6844=ORIENTED_EDGE('',*,*,#5045,.F.);
#6845=ORIENTED_EDGE('',*,*,#5050,.T.);
#6846=ORIENTED_EDGE('',*,*,#5051,.T.);
#6847=ORIENTED_EDGE('',*,*,#5052,.T.);
#6848=ORIENTED_EDGE('',*,*,#5048,.F.);
#6849=ORIENTED_EDGE('',*,*,#5053,.T.);
#6850=ORIENTED_EDGE('',*,*,#5040,.T.);
#6851=ORIENTED_EDGE('',*,*,#5054,.T.);
#6852=ORIENTED_EDGE('',*,*,#5051,.F.);
#6853=ORIENTED_EDGE('',*,*,#5053,.F.);
#6854=ORIENTED_EDGE('',*,*,#5050,.F.);
#6855=ORIENTED_EDGE('',*,*,#5047,.F.);
#6856=ORIENTED_EDGE('',*,*,#5044,.F.);
#6857=ORIENTED_EDGE('',*,*,#5041,.F.);
#6858=ORIENTED_EDGE('',*,*,#5037,.F.);
#6859=ORIENTED_EDGE('',*,*,#5054,.F.);
#6860=ORIENTED_EDGE('',*,*,#5039,.F.);
#6861=ORIENTED_EDGE('',*,*,#5043,.F.);
#6862=ORIENTED_EDGE('',*,*,#5046,.F.);
#6863=ORIENTED_EDGE('',*,*,#5049,.F.);
#6864=ORIENTED_EDGE('',*,*,#5052,.F.);
#6865=ORIENTED_EDGE('',*,*,#5055,.F.);
#6866=ORIENTED_EDGE('',*,*,#5056,.F.);
#6867=ORIENTED_EDGE('',*,*,#5057,.F.);
#6868=ORIENTED_EDGE('',*,*,#5058,.T.);
#6869=ORIENTED_EDGE('',*,*,#5056,.T.);
#6870=ORIENTED_EDGE('',*,*,#5058,.F.);
#6871=ORIENTED_EDGE('',*,*,#5059,.F.);
#6872=ORIENTED_EDGE('',*,*,#5060,.T.);
#6873=ORIENTED_EDGE('',*,*,#5057,.T.);
#6874=ORIENTED_EDGE('',*,*,#5060,.F.);
#6875=ORIENTED_EDGE('',*,*,#5061,.F.);
#6876=ORIENTED_EDGE('',*,*,#5062,.T.);
#6877=ORIENTED_EDGE('',*,*,#5059,.T.);
#6878=ORIENTED_EDGE('',*,*,#5062,.F.);
#6879=ORIENTED_EDGE('',*,*,#5061,.T.);
#6880=ORIENTED_EDGE('',*,*,#5063,.F.);
#6881=ORIENTED_EDGE('',*,*,#5064,.F.);
#6882=ORIENTED_EDGE('',*,*,#5065,.T.);
#6883=ORIENTED_EDGE('',*,*,#5063,.T.);
#6884=ORIENTED_EDGE('',*,*,#5065,.F.);
#6885=ORIENTED_EDGE('',*,*,#5055,.T.);
#6886=ORIENTED_EDGE('',*,*,#5066,.T.);
#6887=ORIENTED_EDGE('',*,*,#5064,.T.);
#6888=ORIENTED_EDGE('',*,*,#5066,.F.);
#6972=CYLINDRICAL_SURFACE('',#8431,0.35);
#6973=CYLINDRICAL_SURFACE('',#8439,0.1954);
#7347=ADVANCED_FACE('',(#1421),#1037,.F.);
#7348=ADVANCED_FACE('',(#1422),#1038,.F.);
#7349=ADVANCED_FACE('',(#1423),#1039,.F.);
#7350=ADVANCED_FACE('',(#1424),#1040,.F.);
#7351=ADVANCED_FACE('',(#1425),#1041,.F.);
#7352=ADVANCED_FACE('',(#1426),#1042,.F.);
#7353=ADVANCED_FACE('',(#1427),#1043,.F.);
#7354=ADVANCED_FACE('',(#1428),#1044,.F.);
#7355=ADVANCED_FACE('',(#1429),#1045,.F.);
#7356=ADVANCED_FACE('',(#1430),#1046,.T.);
#7357=ADVANCED_FACE('',(#1431),#515,.T.);
#7358=ADVANCED_FACE('',(#1432),#6972,.T.);
#7359=ADVANCED_FACE('',(#1433),#516,.T.);
#7360=ADVANCED_FACE('',(#1434,#763),#1047,.T.);
#7361=ADVANCED_FACE('',(#1435),#517,.T.);
#7362=ADVANCED_FACE('',(#1436),#6973,.T.);
#7397=CLOSED_SHELL('',(#7347,#7348,#7349,#7350,#7351,#7352,#7353,#7354));
#7398=CLOSED_SHELL('',(#7355,#7356,#7357,#7358,#7359,#7360,#7361,#7362));
#8416=AXIS2_PLACEMENT_3D('',#12620,#10523,#10524);
#8417=AXIS2_PLACEMENT_3D('',#12621,#10525,#10526);
#8418=AXIS2_PLACEMENT_3D('',#12630,#10531,#10532);
#8419=AXIS2_PLACEMENT_3D('',#12636,#10536,#10537);
#8420=AXIS2_PLACEMENT_3D('',#12642,#10541,#10542);
#8421=AXIS2_PLACEMENT_3D('',#12648,#10546,#10547);
#8422=AXIS2_PLACEMENT_3D('',#12654,#10551,#10552);
#8423=AXIS2_PLACEMENT_3D('',#12657,#10555,#10556);
#8424=AXIS2_PLACEMENT_3D('',#12658,#10557,#10558);
#8425=AXIS2_PLACEMENT_3D('',#12659,#10559,#10560);
#8426=AXIS2_PLACEMENT_3D('',#12661,#10561,#10562);
#8427=AXIS2_PLACEMENT_3D('',#12662,#10563,#10564);
#8428=AXIS2_PLACEMENT_3D('',#12664,#10565,#10566);
#8429=AXIS2_PLACEMENT_3D('',#12665,#10567,#10568);
#8430=AXIS2_PLACEMENT_3D('',#12667,#10569,#10570);
#8431=AXIS2_PLACEMENT_3D('',#12669,#10572,#10573);
#8432=AXIS2_PLACEMENT_3D('',#12671,#10574,#10575);
#8433=AXIS2_PLACEMENT_3D('',#12673,#10577,#10578);
#8434=AXIS2_PLACEMENT_3D('',#12675,#10579,#10580);
#8435=AXIS2_PLACEMENT_3D('',#12677,#10582,#10583);
#8436=AXIS2_PLACEMENT_3D('',#12679,#10584,#10585);
#8437=AXIS2_PLACEMENT_3D('',#12680,#10586,#10587);
#8438=AXIS2_PLACEMENT_3D('',#12682,#10588,#10589);
#8439=AXIS2_PLACEMENT_3D('',#12684,#10591,#10592);
#10523=DIRECTION('axis',(0.,0.,1.));
#10524=DIRECTION('refdir',(1.,0.,0.));
#10525=DIRECTION('center_axis',(0.866025403784439,0.,-0.5));
#10526=DIRECTION('ref_axis',(0.5,0.,0.866025403784439));
#10527=DIRECTION('',(-0.5,0.,-0.866025403784439));
#10528=DIRECTION('',(0.,-1.,0.));
#10529=DIRECTION('',(0.5,0.,0.866025403784439));
#10530=DIRECTION('',(0.,-1.,0.));
#10531=DIRECTION('center_axis',(1.60246890531964E-16,0.,-1.));
#10532=DIRECTION('ref_axis',(1.,0.,1.60246890531964E-16));
#10533=DIRECTION('',(-1.,0.,-1.60246890531964E-16));
#10534=DIRECTION('',(0.,-1.,0.));
#10535=DIRECTION('',(1.,0.,1.60246890531964E-16));
#10536=DIRECTION('center_axis',(-0.866025403784439,0.,-0.5));
#10537=DIRECTION('ref_axis',(0.5,0.,-0.866025403784439));
#10538=DIRECTION('',(-0.5,0.,0.866025403784439));
#10539=DIRECTION('',(0.,-1.,0.));
#10540=DIRECTION('',(0.5,0.,-0.866025403784439));
#10541=DIRECTION('center_axis',(-0.866025403784439,0.,0.5));
#10542=DIRECTION('ref_axis',(-0.5,0.,-0.866025403784439));
#10543=DIRECTION('',(0.5,0.,0.866025403784439));
#10544=DIRECTION('',(0.,-1.,0.));
#10545=DIRECTION('',(-0.5,0.,-0.866025403784439));
#10546=DIRECTION('center_axis',(-1.60246890531964E-16,0.,1.));
#10547=DIRECTION('ref_axis',(-1.,0.,-1.60246890531964E-16));
#10548=DIRECTION('',(1.,0.,1.60246890531964E-16));
#10549=DIRECTION('',(0.,-1.,0.));
#10550=DIRECTION('',(-1.,0.,-1.60246890531964E-16));
#10551=DIRECTION('center_axis',(0.866025403784439,0.,0.5));
#10552=DIRECTION('ref_axis',(-0.5,0.,0.866025403784439));
#10553=DIRECTION('',(0.5,0.,-0.866025403784439));
#10554=DIRECTION('',(-0.5,0.,0.866025403784439));
#10555=DIRECTION('center_axis',(0.,1.,0.));
#10556=DIRECTION('ref_axis',(1.,0.,0.));
#10557=DIRECTION('center_axis',(0.,-1.,0.));
#10558=DIRECTION('ref_axis',(0.,0.,-1.));
#10559=DIRECTION('center_axis',(0.,1.,0.));
#10560=DIRECTION('ref_axis',(1.,0.,0.));
#10561=DIRECTION('center_axis',(0.,1.,0.));
#10562=DIRECTION('ref_axis',(1.,0.,0.));
#10563=DIRECTION('center_axis',(0.,1.,0.));
#10564=DIRECTION('ref_axis',(0.,0.,1.));
#10565=DIRECTION('center_axis',(0.,-1.,0.));
#10566=DIRECTION('ref_axis',(1.,0.,0.));
#10567=DIRECTION('center_axis',(0.,-1.,0.));
#10568=DIRECTION('ref_axis',(1.,0.,0.));
#10569=DIRECTION('center_axis',(0.,-1.,0.));
#10570=DIRECTION('ref_axis',(1.,0.,0.));
#10571=DIRECTION('',(0.707106781186547,0.707106781186548,8.65956056235493E-17));
#10572=DIRECTION('center_axis',(0.,-1.,0.));
#10573=DIRECTION('ref_axis',(1.,0.,0.));
#10574=DIRECTION('center_axis',(0.,-1.,0.));
#10575=DIRECTION('ref_axis',(1.,0.,0.));
#10576=DIRECTION('',(0.,1.,0.));
#10577=DIRECTION('center_axis',(0.,1.,0.));
#10578=DIRECTION('ref_axis',(1.,0.,0.));
#10579=DIRECTION('center_axis',(0.,-1.,0.));
#10580=DIRECTION('ref_axis',(1.,0.,0.));
#10581=DIRECTION('',(-0.707106781186547,0.707106781186548,-8.65956056235493E-17));
#10582=DIRECTION('center_axis',(0.,-1.,0.));
#10583=DIRECTION('ref_axis',(0.,0.,-1.));
#10584=DIRECTION('center_axis',(0.,-1.,0.));
#10585=DIRECTION('ref_axis',(1.,0.,0.));
#10586=DIRECTION('center_axis',(0.,1.,0.));
#10587=DIRECTION('ref_axis',(1.,0.,0.));
#10588=DIRECTION('center_axis',(0.,1.,0.));
#10589=DIRECTION('ref_axis',(1.,0.,0.));
#10590=DIRECTION('',(-0.447213595499958,0.894427190999916,-5.47678698264203E-17));
#10591=DIRECTION('center_axis',(0.,-1.,0.));
#10592=DIRECTION('ref_axis',(1.,0.,0.));
#10593=DIRECTION('',(0.,1.,0.));
#12620=CARTESIAN_POINT('',(0.,0.,0.));
#12621=CARTESIAN_POINT('Origin',(0.0866025403784439,-0.4,-0.15));
#12622=CARTESIAN_POINT('',(0.173205080756888,-0.4,0.));
#12623=CARTESIAN_POINT('',(0.0866025403784439,-0.4,-0.15));
#12624=CARTESIAN_POINT('',(0.173205080756888,-0.4,0.));
#12625=CARTESIAN_POINT('',(0.0866025403784439,-0.64,-0.15));
#12626=CARTESIAN_POINT('',(0.0866025403784439,-0.4,-0.15));
#12627=CARTESIAN_POINT('',(0.173205080756888,-0.64,0.));
#12628=CARTESIAN_POINT('',(0.173205080756888,-0.64,0.));
#12629=CARTESIAN_POINT('',(0.173205080756888,-0.4,0.));
#12630=CARTESIAN_POINT('Origin',(-0.0866025403784438,-0.4,-0.15));
#12631=CARTESIAN_POINT('',(-0.0866025403784438,-0.4,-0.15));
#12632=CARTESIAN_POINT('',(0.0866025403784439,-0.4,-0.15));
#12633=CARTESIAN_POINT('',(-0.0866025403784438,-0.64,-0.15));
#12634=CARTESIAN_POINT('',(-0.0866025403784438,-0.4,-0.15));
#12635=CARTESIAN_POINT('',(0.0866025403784439,-0.64,-0.15));
#12636=CARTESIAN_POINT('Origin',(-0.173205080756888,-0.4,-2.77555756156289E-17));
#12637=CARTESIAN_POINT('',(-0.173205080756888,-0.4,-2.12115047744981E-17));
#12638=CARTESIAN_POINT('',(-0.0866025403784438,-0.4,-0.15));
#12639=CARTESIAN_POINT('',(-0.173205080756888,-0.64,-2.77555756156289E-17));
#12640=CARTESIAN_POINT('',(-0.173205080756888,-0.4,-2.12115047744981E-17));
#12641=CARTESIAN_POINT('',(-0.0866025403784438,-0.64,-0.15));
#12642=CARTESIAN_POINT('Origin',(-0.0866025403784439,-0.4,0.15));
#12643=CARTESIAN_POINT('',(-0.0866025403784439,-0.4,0.15));
#12644=CARTESIAN_POINT('',(-0.173205080756888,-0.4,-2.12115047744981E-17));
#12645=CARTESIAN_POINT('',(-0.0866025403784439,-0.64,0.15));
#12646=CARTESIAN_POINT('',(-0.0866025403784439,-0.4,0.15));
#12647=CARTESIAN_POINT('',(-0.173205080756888,-0.64,-2.12115047744981E-17));
#12648=CARTESIAN_POINT('Origin',(0.0866025403784439,-0.4,0.15));
#12649=CARTESIAN_POINT('',(0.0866025403784439,-0.4,0.15));
#12650=CARTESIAN_POINT('',(-0.0866025403784439,-0.4,0.15));
#12651=CARTESIAN_POINT('',(0.0866025403784439,-0.64,0.15));
#12652=CARTESIAN_POINT('',(0.0866025403784439,-0.4,0.15));
#12653=CARTESIAN_POINT('',(-0.0866025403784439,-0.64,0.15));
#12654=CARTESIAN_POINT('Origin',(0.173205080756888,-0.4,0.));
#12655=CARTESIAN_POINT('',(0.0866025403784439,-0.4,0.15));
#12656=CARTESIAN_POINT('',(0.0866025403784439,-0.64,0.15));
#12657=CARTESIAN_POINT('Origin',(0.,-0.4,-2.77555756156289E-17));
#12658=CARTESIAN_POINT('Origin',(0.,-0.64,-2.77555756156289E-17));
#12659=CARTESIAN_POINT('Origin',(0.,-1.,0.));
#12660=CARTESIAN_POINT('',(-0.1954,-1.,2.39295984553393E-17));
#12661=CARTESIAN_POINT('Origin',(0.,-1.,0.));
#12662=CARTESIAN_POINT('Origin',(0.3,0.4,0.));
#12663=CARTESIAN_POINT('',(-0.3,0.4,-3.67394039744206E-17));
#12664=CARTESIAN_POINT('Origin',(0.,0.4,0.));
#12665=CARTESIAN_POINT('Origin',(0.,0.375,0.));
#12666=CARTESIAN_POINT('',(-0.35,0.35,-4.28626379701573E-17));
#12667=CARTESIAN_POINT('Origin',(0.,0.35,0.));
#12668=CARTESIAN_POINT('',(-0.325,0.375,-3.9801020972289E-17));
#12669=CARTESIAN_POINT('Origin',(0.,0.19,0.));
#12670=CARTESIAN_POINT('',(-0.35,0.03,-4.28626379701574E-17));
#12671=CARTESIAN_POINT('Origin',(0.,0.03,0.));
#12672=CARTESIAN_POINT('',(-0.35,0.19,-4.28626379701574E-17));
#12673=CARTESIAN_POINT('Origin',(0.,0.0149999999999999,0.));
#12674=CARTESIAN_POINT('',(-0.32,-3.29597460435593E-17,-3.91886975727153E-17));
#12675=CARTESIAN_POINT('Origin',(0.,0.,0.));
#12676=CARTESIAN_POINT('',(-0.335,0.0149999999999999,-4.10256677714363E-17));
#12677=CARTESIAN_POINT('Origin',(0.22,0.,0.));
#12678=CARTESIAN_POINT('',(-0.22,-6.93889390390723E-18,-2.69422295812418E-17));
#12679=CARTESIAN_POINT('Origin',(0.,0.,0.));
#12680=CARTESIAN_POINT('Origin',(0.,-0.02,0.));
#12681=CARTESIAN_POINT('',(-0.1954,-0.0492,2.39295984553393E-17));
#12682=CARTESIAN_POINT('Origin',(0.,-0.0492,0.));
#12683=CARTESIAN_POINT('',(-0.21,-0.02,-2.57175827820944E-17));
#12684=CARTESIAN_POINT('Origin',(0.,-0.8,0.));
#12685=CARTESIAN_POINT('',(-0.1954,-0.8,-2.39295984553393E-17));
#12767=UNCERTAINTY_MEASURE_WITH_UNIT(LENGTH_MEASURE(0.001),#12805,
'DISTANCE_ACCURACY_VALUE',
'Maximum model space distance between geometric entities at asserted c
onnectivities');
#12768=UNCERTAINTY_MEASURE_WITH_UNIT(LENGTH_MEASURE(0.001),#12805,
'DISTANCE_ACCURACY_VALUE',
'Maximum model space distance between geometric entities at asserted c
onnectivities');
#12803=(
GEOMETRIC_REPRESENTATION_CONTEXT(3)
GLOBAL_UNCERTAINTY_ASSIGNED_CONTEXT((#12767))
GLOBAL_UNIT_ASSIGNED_CONTEXT((#12805,#12807,#12808))
REPRESENTATION_CONTEXT('','3D')
);
#12804=(
GEOMETRIC_REPRESENTATION_CONTEXT(3)
GLOBAL_UNCERTAINTY_ASSIGNED_CONTEXT((#12768))
GLOBAL_UNIT_ASSIGNED_CONTEXT((#12805,#12807,#12808))
REPRESENTATION_CONTEXT('','3D')
);
#12805=(
LENGTH_UNIT()
NAMED_UNIT(*)
SI_UNIT(.CENTI.,.METRE.)
);
#12807=(
NAMED_UNIT(*)
PLANE_ANGLE_UNIT()
SI_UNIT($,.RADIAN.)
);
#12808=(
NAMED_UNIT(*)
SI_UNIT($,.STERADIAN.)
SOLID_ANGLE_UNIT()
);
#12843=SHAPE_DEFINITION_REPRESENTATION(#12951,#13033);
#12951=PRODUCT_DEFINITION_SHAPE('',$,#13069);
#13033=SHAPE_REPRESENTATION('',(#8416),#12803);
#13034=PRODUCT_DEFINITION_CONTEXT('part definition',#13141,'design');
#13069=PRODUCT_DEFINITION('M4x10 Cap Screw','M4x10 Cap Screw',#13104,#13034);
#13104=PRODUCT_DEFINITION_FORMATION('',$,#13177);
#13141=APPLICATION_CONTEXT(
'Core Data for Automotive Mechanical Design Process');
#13142=PRODUCT_CONTEXT('part definition',#13141,'mechanical');
#13177=PRODUCT('M4x10 Cap Screw','M4x10 Cap Screw','M4x10 Cap Screw',(#13142));
#13248=COLOUR_RGB('Black',0.12,0.14,0.17);
#13249=FILL_AREA_STYLE_COLOUR('',#13248);
#13250=FILL_AREA_STYLE('',(#13249));
#13251=SURFACE_STYLE_FILL_AREA(#13250);
#13252=SURFACE_SIDE_STYLE('',(#13251));
#13253=SURFACE_STYLE_USAGE(.BOTH.,#13252);
#13254=PRESENTATION_STYLE_ASSIGNMENT((#13253));
ENDSEC;
END-ISO-10303-21;
